ISO-10303-21;
HEADER;
/* Generated by software containing ST-Developer
 * from STEP Tools, Inc. (www.steptools.com) 
 */

FILE_DESCRIPTION(
/* description */ ('PAT-091'),
/* implementation_level */ '2;1');

FILE_NAME(
/* name */ 'Screw bearing cap (3).step',
/* time_stamp */ '2026-10-27T15:34:44-07:00',
/* author */ (''),
/* organization */ (''),
/* preprocessor_version */ 'ST-DEVELOPER v20.2',
/* originating_system */ 'Autodesk Translation Framework v15.17.0.0',
/* authorisation */ '');

FILE_SCHEMA (('AUTOMOTIVE_DESIGN { 1 0 10303 214 3 1 1 }'));
ENDSEC;

DATA;
#10=MECHANICAL_DESIGN_GEOMETRIC_PRESENTATION_REPRESENTATION('',(#979),#25100);
#759=SHAPE_REPRESENTATION_RELATIONSHIP('SRR','None',#25520,#869);
#869=ADVANCED_BREP_SHAPE_REPRESENTATION('',(#1103),#24990);
#979=STYLED_ITEM('',(#26198),#1103);
#1103=MANIFOLD_SOLID_BREP('Body1',#13256);
#1310=FACE_BOUND('',#3081,.T.);
#1311=FACE_BOUND('',#3085,.T.);
#1312=FACE_BOUND('',#3086,.T.);
#1313=FACE_BOUND('',#3087,.T.);
#1314=FACE_BOUND('',#3088,.T.);
#1315=FACE_BOUND('',#3089,.T.);
#1316=FACE_BOUND('',#3091,.T.);
#1317=FACE_BOUND('',#3092,.T.);
#1318=FACE_BOUND('',#3093,.T.);
#1319=FACE_BOUND('',#3094,.T.);
#1320=FACE_BOUND('',#3095,.T.);
#1687=PLANE('',#14814);
#1688=PLANE('',#14821);
#1689=PLANE('',#14822);
#2162=FACE_OUTER_BOUND('',#3075,.T.);
#2163=FACE_OUTER_BOUND('',#3076,.T.);
#2164=FACE_OUTER_BOUND('',#3077,.T.);
#2165=FACE_OUTER_BOUND('',#3078,.T.);
#2166=FACE_OUTER_BOUND('',#3079,.T.);
#2167=FACE_OUTER_BOUND('',#3080,.T.);
#2168=FACE_OUTER_BOUND('',#3082,.T.);
#2169=FACE_OUTER_BOUND('',#3083,.T.);
#2170=FACE_OUTER_BOUND('',#3084,.T.);
#2171=FACE_OUTER_BOUND('',#3090,.T.);
#3075=EDGE_LOOP('',(#9452,#9453,#9454,#9455));
#3076=EDGE_LOOP('',(#9456,#9457,#9458,#9459));
#3077=EDGE_LOOP('',(#9460,#9461,#9462,#9463));
#3078=EDGE_LOOP('',(#9464,#9465,#9466,#9467));
#3079=EDGE_LOOP('',(#9468,#9469,#9470,#9471));
#3080=EDGE_LOOP('',(#9472));
#3081=EDGE_LOOP('',(#9473));
#3082=EDGE_LOOP('',(#9474,#9475,#9476,#9477));
#3083=EDGE_LOOP('',(#9478,#9479,#9480,#9481));
#3084=EDGE_LOOP('',(#9482));
#3085=EDGE_LOOP('',(#9483));
#3086=EDGE_LOOP('',(#9484));
#3087=EDGE_LOOP('',(#9485));
#3088=EDGE_LOOP('',(#9486));
#3089=EDGE_LOOP('',(#9487));
#3090=EDGE_LOOP('',(#9488));
#3091=EDGE_LOOP('',(#9489));
#3092=EDGE_LOOP('',(#9490));
#3093=EDGE_LOOP('',(#9491));
#3094=EDGE_LOOP('',(#9492));
#3095=EDGE_LOOP('',(#9493));
#4260=LINE('',#21488,#5000);
#4261=LINE('',#21494,#5001);
#4262=LINE('',#21500,#5002);
#4263=LINE('',#21506,#5003);
#4264=LINE('',#21512,#5004);
#4265=LINE('',#21520,#5005);
#4266=LINE('',#21525,#5006);
#5000=VECTOR('',#17036,0.225);
#5001=VECTOR('',#17043,0.225);
#5002=VECTOR('',#17050,0.225);
#5003=VECTOR('',#17057,0.225);
#5004=VECTOR('',#17064,1.59);
#5005=VECTOR('',#17075,1.02);
#5006=VECTOR('',#17080,2.2);
#5708=CIRCLE('',#14800,0.225);
#5709=CIRCLE('',#14801,0.225);
#5710=CIRCLE('',#14803,0.225);
#5711=CIRCLE('',#14804,0.225);
#5712=CIRCLE('',#14806,0.225);
#5713=CIRCLE('',#14807,0.225);
#5714=CIRCLE('',#14809,0.225);
#5715=CIRCLE('',#14810,0.225);
#5716=CIRCLE('',#14812,1.59);
#5717=CIRCLE('',#14813,1.59);
#5718=CIRCLE('',#14815,1.02);
#5719=CIRCLE('',#14817,1.02);
#5720=CIRCLE('',#14819,2.2);
#5721=CIRCLE('',#14820,2.2);
#6543=VERTEX_POINT('',#21485);
#6544=VERTEX_POINT('',#21487);
#6545=VERTEX_POINT('',#21491);
#6546=VERTEX_POINT('',#21493);
#6547=VERTEX_POINT('',#21497);
#6548=VERTEX_POINT('',#21499);
#6549=VERTEX_POINT('',#21503);
#6550=VERTEX_POINT('',#21505);
#6551=VERTEX_POINT('',#21509);
#6552=VERTEX_POINT('',#21511);
#6553=VERTEX_POINT('',#21515);
#6554=VERTEX_POINT('',#21518);
#6555=VERTEX_POINT('',#21522);
#6556=VERTEX_POINT('',#21524);
#7661=EDGE_CURVE('',#6543,#6543,#5708,.T.);
#7662=EDGE_CURVE('',#6543,#6544,#4260,.T.);
#7663=EDGE_CURVE('',#6544,#6544,#5709,.T.);
#7664=EDGE_CURVE('',#6545,#6545,#5710,.T.);
#7665=EDGE_CURVE('',#6545,#6546,#4261,.T.);
#7666=EDGE_CURVE('',#6546,#6546,#5711,.T.);
#7667=EDGE_CURVE('',#6547,#6547,#5712,.T.);
#7668=EDGE_CURVE('',#6547,#6548,#4262,.T.);
#7669=EDGE_CURVE('',#6548,#6548,#5713,.T.);
#7670=EDGE_CURVE('',#6549,#6549,#5714,.T.);
#7671=EDGE_CURVE('',#6549,#6550,#4263,.T.);
#7672=EDGE_CURVE('',#6550,#6550,#5715,.T.);
#7673=EDGE_CURVE('',#6551,#6551,#5716,.T.);
#7674=EDGE_CURVE('',#6551,#6552,#4264,.T.);
#7675=EDGE_CURVE('',#6552,#6552,#5717,.T.);
#7676=EDGE_CURVE('',#6553,#6553,#5718,.T.);
#7677=EDGE_CURVE('',#6554,#6554,#5719,.T.);
#7678=EDGE_CURVE('',#6554,#6553,#4265,.T.);
#7679=EDGE_CURVE('',#6555,#6555,#5720,.T.);
#7680=EDGE_CURVE('',#6555,#6556,#4266,.T.);
#7681=EDGE_CURVE('',#6556,#6556,#5721,.T.);
#9452=ORIENTED_EDGE('',*,*,#7661,.F.);
#9453=ORIENTED_EDGE('',*,*,#7662,.T.);
#9454=ORIENTED_EDGE('',*,*,#7663,.F.);
#9455=ORIENTED_EDGE('',*,*,#7662,.F.);
#9456=ORIENTED_EDGE('',*,*,#7664,.F.);
#9457=ORIENTED_EDGE('',*,*,#7665,.T.);
#9458=ORIENTED_EDGE('',*,*,#7666,.F.);
#9459=ORIENTED_EDGE('',*,*,#7665,.F.);
#9460=ORIENTED_EDGE('',*,*,#7667,.F.);
#9461=ORIENTED_EDGE('',*,*,#7668,.T.);
#9462=ORIENTED_EDGE('',*,*,#7669,.F.);
#9463=ORIENTED_EDGE('',*,*,#7668,.F.);
#9464=ORIENTED_EDGE('',*,*,#7670,.F.);
#9465=ORIENTED_EDGE('',*,*,#7671,.T.);
#9466=ORIENTED_EDGE('',*,*,#7672,.F.);
#9467=ORIENTED_EDGE('',*,*,#7671,.F.);
#9468=ORIENTED_EDGE('',*,*,#7673,.F.);
#9469=ORIENTED_EDGE('',*,*,#7674,.T.);
#9470=ORIENTED_EDGE('',*,*,#7675,.T.);
#9471=ORIENTED_EDGE('',*,*,#7674,.F.);
#9472=ORIENTED_EDGE('',*,*,#7675,.F.);
#9473=ORIENTED_EDGE('',*,*,#7676,.F.);
#9474=ORIENTED_EDGE('',*,*,#7677,.F.);
#9475=ORIENTED_EDGE('',*,*,#7678,.T.);
#9476=ORIENTED_EDGE('',*,*,#7676,.T.);
#9477=ORIENTED_EDGE('',*,*,#7678,.F.);
#9478=ORIENTED_EDGE('',*,*,#7679,.F.);
#9479=ORIENTED_EDGE('',*,*,#7680,.T.);
#9480=ORIENTED_EDGE('',*,*,#7681,.T.);
#9481=ORIENTED_EDGE('',*,*,#7680,.F.);
#9482=ORIENTED_EDGE('',*,*,#7679,.T.);
#9483=ORIENTED_EDGE('',*,*,#7677,.T.);
#9484=ORIENTED_EDGE('',*,*,#7672,.T.);
#9485=ORIENTED_EDGE('',*,*,#7669,.T.);
#9486=ORIENTED_EDGE('',*,*,#7666,.T.);
#9487=ORIENTED_EDGE('',*,*,#7663,.T.);
#9488=ORIENTED_EDGE('',*,*,#7681,.F.);
#9489=ORIENTED_EDGE('',*,*,#7673,.T.);
#9490=ORIENTED_EDGE('',*,*,#7670,.T.);
#9491=ORIENTED_EDGE('',*,*,#7667,.T.);
#9492=ORIENTED_EDGE('',*,*,#7664,.T.);
#9493=ORIENTED_EDGE('',*,*,#7661,.T.);
#12126=CYLINDRICAL_SURFACE('',#14799,0.225);
#12127=CYLINDRICAL_SURFACE('',#14802,0.225);
#12128=CYLINDRICAL_SURFACE('',#14805,0.225);
#12129=CYLINDRICAL_SURFACE('',#14808,0.225);
#12130=CYLINDRICAL_SURFACE('',#14811,1.59);
#12131=CYLINDRICAL_SURFACE('',#14816,1.02);
#12132=CYLINDRICAL_SURFACE('',#14818,2.2);
#12529=ADVANCED_FACE('',(#2162),#12126,.F.);
#12530=ADVANCED_FACE('',(#2163),#12127,.F.);
#12531=ADVANCED_FACE('',(#2164),#12128,.F.);
#12532=ADVANCED_FACE('',(#2165),#12129,.F.);
#12533=ADVANCED_FACE('',(#2166),#12130,.T.);
#12534=ADVANCED_FACE('',(#2167,#1310),#1687,.F.);
#12535=ADVANCED_FACE('',(#2168),#12131,.F.);
#12536=ADVANCED_FACE('',(#2169),#12132,.T.);
#12537=ADVANCED_FACE('',(#2170,#1311,#1312,#1313,#1314,#1315),#1688,.T.);
#12538=ADVANCED_FACE('',(#2171,#1316,#1317,#1318,#1319,#1320),#1689,.F.);
#13256=CLOSED_SHELL('',(#12529,#12530,#12531,#12532,#12533,#12534,#12535,
#12536,#12537,#12538));
#14798=AXIS2_PLACEMENT_3D('',#21483,#17030,#17031);
#14799=AXIS2_PLACEMENT_3D('',#21484,#17032,#17033);
#14800=AXIS2_PLACEMENT_3D('',#21486,#17034,#17035);
#14801=AXIS2_PLACEMENT_3D('',#21489,#17037,#17038);
#14802=AXIS2_PLACEMENT_3D('',#21490,#17039,#17040);
#14803=AXIS2_PLACEMENT_3D('',#21492,#17041,#17042);
#14804=AXIS2_PLACEMENT_3D('',#21495,#17044,#17045);
#14805=AXIS2_PLACEMENT_3D('',#21496,#17046,#17047);
#14806=AXIS2_PLACEMENT_3D('',#21498,#17048,#17049);
#14807=AXIS2_PLACEMENT_3D('',#21501,#17051,#17052);
#14808=AXIS2_PLACEMENT_3D('',#21502,#17053,#17054);
#14809=AXIS2_PLACEMENT_3D('',#21504,#17055,#17056);
#14810=AXIS2_PLACEMENT_3D('',#21507,#17058,#17059);
#14811=AXIS2_PLACEMENT_3D('',#21508,#17060,#17061);
#14812=AXIS2_PLACEMENT_3D('',#21510,#17062,#17063);
#14813=AXIS2_PLACEMENT_3D('',#21513,#17065,#17066);
#14814=AXIS2_PLACEMENT_3D('',#21514,#17067,#17068);
#14815=AXIS2_PLACEMENT_3D('',#21516,#17069,#17070);
#14816=AXIS2_PLACEMENT_3D('',#21517,#17071,#17072);
#14817=AXIS2_PLACEMENT_3D('',#21519,#17073,#17074);
#14818=AXIS2_PLACEMENT_3D('',#21521,#17076,#17077);
#14819=AXIS2_PLACEMENT_3D('',#21523,#17078,#17079);
#14820=AXIS2_PLACEMENT_3D('',#21526,#17081,#17082);
#14821=AXIS2_PLACEMENT_3D('',#21527,#17083,#17084);
#14822=AXIS2_PLACEMENT_3D('',#21528,#17085,#17086);
#17030=DIRECTION('axis',(0.,0.,1.));
#17031=DIRECTION('refdir',(1.,0.,0.));
#17032=DIRECTION('center_axis',(1.,0.,0.));
#17033=DIRECTION('ref_axis',(0.,0.,-1.));
#17034=DIRECTION('center_axis',(1.,0.,0.));
#17035=DIRECTION('ref_axis',(0.,0.,-1.));
#17036=DIRECTION('',(1.,0.,0.));
#17037=DIRECTION('center_axis',(-1.,0.,0.));
#17038=DIRECTION('ref_axis',(0.,0.,-1.));
#17039=DIRECTION('center_axis',(1.,0.,0.));
#17040=DIRECTION('ref_axis',(0.,0.,-1.));
#17041=DIRECTION('center_axis',(1.,0.,0.));
#17042=DIRECTION('ref_axis',(0.,0.,-1.));
#17043=DIRECTION('',(1.,0.,0.));
#17044=DIRECTION('center_axis',(-1.,0.,0.));
#17045=DIRECTION('ref_axis',(0.,0.,-1.));
#17046=DIRECTION('center_axis',(1.,0.,0.));
#17047=DIRECTION('ref_axis',(0.,0.,-1.));
#17048=DIRECTION('center_axis',(1.,0.,0.));
#17049=DIRECTION('ref_axis',(0.,0.,-1.));
#17050=DIRECTION('',(1.,0.,0.));
#17051=DIRECTION('center_axis',(-1.,0.,0.));
#17052=DIRECTION('ref_axis',(0.,0.,-1.));
#17053=DIRECTION('center_axis',(1.,0.,0.));
#17054=DIRECTION('ref_axis',(0.,0.,-1.));
#17055=DIRECTION('center_axis',(1.,0.,0.));
#17056=DIRECTION('ref_axis',(0.,0.,-1.));
#17057=DIRECTION('',(1.,0.,0.));
#17058=DIRECTION('center_axis',(-1.,0.,0.));
#17059=DIRECTION('ref_axis',(0.,0.,-1.));
#17060=DIRECTION('center_axis',(1.,0.,0.));
#17061=DIRECTION('ref_axis',(0.,0.,-1.));
#17062=DIRECTION('center_axis',(1.,0.,0.));
#17063=DIRECTION('ref_axis',(0.,0.,-1.));
#17064=DIRECTION('',(-1.,0.,0.));
#17065=DIRECTION('center_axis',(1.,0.,0.));
#17066=DIRECTION('ref_axis',(0.,0.,-1.));
#17067=DIRECTION('center_axis',(1.,0.,0.));
#17068=DIRECTION('ref_axis',(0.,0.,-1.));
#17069=DIRECTION('center_axis',(-1.,0.,0.));
#17070=DIRECTION('ref_axis',(0.,0.,-1.));
#17071=DIRECTION('center_axis',(1.,0.,0.));
#17072=DIRECTION('ref_axis',(0.,0.,-1.));
#17073=DIRECTION('center_axis',(-1.,0.,0.));
#17074=DIRECTION('ref_axis',(0.,0.,-1.));
#17075=DIRECTION('',(-1.,0.,0.));
#17076=DIRECTION('center_axis',(1.,0.,0.));
#17077=DIRECTION('ref_axis',(0.,0.,-1.));
#17078=DIRECTION('center_axis',(1.,0.,0.));
#17079=DIRECTION('ref_axis',(0.,0.,-1.));
#17080=DIRECTION('',(-1.,0.,0.));
#17081=DIRECTION('center_axis',(1.,0.,0.));
#17082=DIRECTION('ref_axis',(0.,0.,-1.));
#17083=DIRECTION('center_axis',(1.,0.,0.));
#17084=DIRECTION('ref_axis',(0.,0.,-1.));
#17085=DIRECTION('center_axis',(1.,0.,0.));
#17086=DIRECTION('ref_axis',(0.,0.,-1.));
#21483=CARTESIAN_POINT('',(0.,0.,0.));
#21484=CARTESIAN_POINT('Origin',(45.9,-1.30814754519511,4.69185245480489));
#21485=CARTESIAN_POINT('',(46.,-1.30814754519511,4.91685245480489));
#21486=CARTESIAN_POINT('Origin',(46.,-1.30814754519511,4.69185245480489));
#21487=CARTESIAN_POINT('',(46.3,-1.30814754519511,4.91685245480489));
#21488=CARTESIAN_POINT('',(45.9,-1.30814754519511,4.91685245480489));
#21489=CARTESIAN_POINT('Origin',(46.3,-1.30814754519511,4.69185245480489));
#21490=CARTESIAN_POINT('Origin',(45.9,-1.30814754519511,7.30814754519511));
#21491=CARTESIAN_POINT('',(46.,-1.30814754519511,7.53314754519511));
#21492=CARTESIAN_POINT('Origin',(46.,-1.30814754519511,7.30814754519511));
#21493=CARTESIAN_POINT('',(46.3,-1.30814754519511,7.53314754519511));
#21494=CARTESIAN_POINT('',(45.9,-1.30814754519511,7.53314754519511));
#21495=CARTESIAN_POINT('Origin',(46.3,-1.30814754519511,7.30814754519511));
#21496=CARTESIAN_POINT('Origin',(45.9,1.30814754519511,7.30814754519511));
#21497=CARTESIAN_POINT('',(46.,1.30814754519511,7.53314754519511));
#21498=CARTESIAN_POINT('Origin',(46.,1.30814754519511,7.30814754519511));
#21499=CARTESIAN_POINT('',(46.3,1.30814754519511,7.53314754519511));
#21500=CARTESIAN_POINT('',(45.9,1.30814754519511,7.53314754519511));
#21501=CARTESIAN_POINT('Origin',(46.3,1.30814754519511,7.30814754519511));
#21502=CARTESIAN_POINT('Origin',(45.9,1.30814754519511,4.69185245480489));
#21503=CARTESIAN_POINT('',(46.,1.30814754519511,4.91685245480489));
#21504=CARTESIAN_POINT('Origin',(46.,1.30814754519511,4.69185245480489));
#21505=CARTESIAN_POINT('',(46.3,1.30814754519511,4.91685245480489));
#21506=CARTESIAN_POINT('',(45.9,1.30814754519511,4.91685245480489));
#21507=CARTESIAN_POINT('Origin',(46.3,1.30814754519511,4.69185245480489));
#21508=CARTESIAN_POINT('Origin',(45.5,0.,6.));
#21509=CARTESIAN_POINT('',(46.,-1.94718841064429E-16,7.59));
#21510=CARTESIAN_POINT('Origin',(46.,0.,6.));
#21511=CARTESIAN_POINT('',(45.5,-1.94718841064429E-16,7.59));
#21512=CARTESIAN_POINT('',(45.5,-1.94718841064429E-16,7.59));
#21513=CARTESIAN_POINT('Origin',(45.5,0.,6.));
#21514=CARTESIAN_POINT('Origin',(45.5,0.,6.));
#21515=CARTESIAN_POINT('',(45.5,-1.2491397351303E-16,7.02));
#21516=CARTESIAN_POINT('Origin',(45.5,0.,6.));
#21517=CARTESIAN_POINT('Origin',(46.,0.,6.));
#21518=CARTESIAN_POINT('',(46.3,-1.2491397351303E-16,7.02));
#21519=CARTESIAN_POINT('Origin',(46.3,0.,6.));
#21520=CARTESIAN_POINT('',(46.,-1.2491397351303E-16,7.02));
#21521=CARTESIAN_POINT('Origin',(46.,0.,6.));
#21522=CARTESIAN_POINT('',(46.3,-2.69422295812418E-16,8.2));
#21523=CARTESIAN_POINT('Origin',(46.3,0.,6.));
#21524=CARTESIAN_POINT('',(46.,-2.69422295812418E-16,8.2));
#21525=CARTESIAN_POINT('',(46.,-2.69422295812418E-16,8.2));
#21526=CARTESIAN_POINT('Origin',(46.,0.,6.));
#21527=CARTESIAN_POINT('Origin',(46.3,0.,6.));
#21528=CARTESIAN_POINT('Origin',(46.,0.,6.));
#24869=UNCERTAINTY_MEASURE_WITH_UNIT(LENGTH_MEASURE(0.001),#25101,
'DISTANCE_ACCURACY_VALUE',
'Maximum model space distance between geometric entities at asserted c
onnectivities');
#24979=UNCERTAINTY_MEASURE_WITH_UNIT(LENGTH_MEASURE(0.001),#25101,
'DISTANCE_ACCURACY_VALUE',
'Maximum model space distance between geometric entities at asserted c
onnectivities');
#24990=(
GEOMETRIC_REPRESENTATION_CONTEXT(3)
GLOBAL_UNCERTAINTY_ASSIGNED_CONTEXT((#24869))
GLOBAL_UNIT_ASSIGNED_CONTEXT((#25101,#25103,#25104))
REPRESENTATION_CONTEXT('','3D')
);
#25100=(
GEOMETRIC_REPRESENTATION_CONTEXT(3)
GLOBAL_UNCERTAINTY_ASSIGNED_CONTEXT((#24979))
GLOBAL_UNIT_ASSIGNED_CONTEXT((#25101,#25103,#25104))
REPRESENTATION_CONTEXT('','3D')
);
#25101=(
LENGTH_UNIT()
NAMED_UNIT(*)
SI_UNIT(.CENTI.,.METRE.)
);
#25103=(
NAMED_UNIT(*)
PLANE_ANGLE_UNIT()
SI_UNIT($,.RADIAN.)
);
#25104=(
NAMED_UNIT(*)
SI_UNIT($,.STERADIAN.)
SOLID_ANGLE_UNIT()
);
#25115=SHAPE_DEFINITION_REPRESENTATION(#25235,#25520);
#25235=PRODUCT_DEFINITION_SHAPE('',$,#25641);
#25520=SHAPE_REPRESENTATION('',(#14798),#24990);
#25630=PRODUCT_DEFINITION_CONTEXT('part definition',#25992,'design');
#25641=PRODUCT_DEFINITION('Screw bearing cap (3)','Screw bearing cap (3)',
#25761,#25630);
#25761=PRODUCT_DEFINITION_FORMATION('',$,#26004);
#25992=APPLICATION_CONTEXT(
'Core Data for Automotive Mechanical Design Process');
#25993=PRODUCT_CONTEXT('part definition',#25992,'mechanical');
#26004=PRODUCT('Screw bearing cap (3)','Screw bearing cap (3)',
'Screw bearing cap (3)',(#25993));
#26192=COLOUR_RGB('Black',0.12,0.14,0.17);
#26193=FILL_AREA_STYLE_COLOUR('',#26192);
#26194=FILL_AREA_STYLE('',(#26193));
#26195=SURFACE_STYLE_FILL_AREA(#26194);
#26196=SURFACE_SIDE_STYLE('',(#26195));
#26197=SURFACE_STYLE_USAGE(.BOTH.,#26196);
#26198=PRESENTATION_STYLE_ASSIGNMENT((#26197));
ENDSEC;
END-ISO-10303-21;
